ISO-10303-21;
HEADER;
/* Generated by software containing ST-Developer
 * from STEP Tools, Inc. (www.steptools.com) 
 */

FILE_DESCRIPTION(
/* description */ (''),
/* implementation_level */ '2;1');

FILE_NAME(
/* name */ 'Arm_04.step',
/* time_stamp */ '2026-10-06T13:41:14-07:00',
/* author */ (''),
/* organization */ (''),
/* preprocessor_version */ 'ST-DEVELOPER v20.2',
/* originating_system */ 'Autodesk Translation Framework v15.15.0.0',
/* authorisation */ '');

FILE_SCHEMA (('AUTOMOTIVE_DESIGN { 1 0 10303 214 3 1 1 }'));
ENDSEC;

DATA;
#10=MECHANICAL_DESIGN_GEOMETRIC_PRESENTATION_REPRESENTATION('',(#1962),#279266);
#1944=SHAPE_REPRESENTATION_RELATIONSHIP('SRR','None',#279303,#1953);
#1953=ADVANCED_BREP_SHAPE_REPRESENTATION('',(#1971),#279259);
#1962=STYLED_ITEM('',(#279355),#1971);
#1971=MANIFOLD_SOLID_BREP('Body1',#14940);
#1989=FACE_BOUND('',#2908,.T.);
#1990=FACE_BOUND('',#2909,.T.);
#1991=FACE_BOUND('',#2911,.T.);
#1992=FACE_BOUND('',#2921,.T.);
#1993=FACE_BOUND('',#2928,.T.);
#1994=FACE_BOUND('',#2929,.T.);
#2051=PLANE('',#15415);
#2052=PLANE('',#15419);
#2053=PLANE('',#15424);
#2054=PLANE('',#15426);
#2055=PLANE('',#15428);
#2056=PLANE('',#15432);
#2057=PLANE('',#15433);
#2058=PLANE('',#15437);
#2059=PLANE('',#15440);
#2060=PLANE('',#15445);
#2423=FACE_OUTER_BOUND('',#2904,.T.);
#2424=FACE_OUTER_BOUND('',#2905,.T.);
#2425=FACE_OUTER_BOUND('',#2906,.T.);
#2426=FACE_OUTER_BOUND('',#2907,.T.);
#2427=FACE_OUTER_BOUND('',#2910,.T.);
#2428=FACE_OUTER_BOUND('',#2912,.T.);
#2429=FACE_OUTER_BOUND('',#2913,.T.);
#2430=FACE_OUTER_BOUND('',#2914,.T.);
#2431=FACE_OUTER_BOUND('',#2915,.T.);
#2432=FACE_OUTER_BOUND('',#2916,.T.);
#2433=FACE_OUTER_BOUND('',#2917,.T.);
#2434=FACE_OUTER_BOUND('',#2918,.T.);
#2435=FACE_OUTER_BOUND('',#2919,.T.);
#2436=FACE_OUTER_BOUND('',#2920,.T.);
#2437=FACE_OUTER_BOUND('',#2922,.T.);
#2438=FACE_OUTER_BOUND('',#2923,.T.);
#2439=FACE_OUTER_BOUND('',#2924,.T.);
#2440=FACE_OUTER_BOUND('',#2925,.T.);
#2441=FACE_OUTER_BOUND('',#2926,.T.);
#2442=FACE_OUTER_BOUND('',#2927,.T.);
#2904=EDGE_LOOP('',(#12956,#12957,#12958,#12959,#12960,#12961,#12962,#12963,
#12964,#12965,#12966,#12967));
#2905=EDGE_LOOP('',(#12968,#12969,#12970,#12971,#12972,#12973,#12974,#12975,
#12976,#12977,#12978,#12979));
#2906=EDGE_LOOP('',(#12980,#12981,#12982,#12983));
#2907=EDGE_LOOP('',(#12984,#12985,#12986,#12987,#12988));
#2908=EDGE_LOOP('',(#12989));
#2909=EDGE_LOOP('',(#12990,#12991,#12992));
#2910=EDGE_LOOP('',(#12993,#12994,#12995,#12996,#12997,#12998));
#2911=EDGE_LOOP('',(#12999));
#2912=EDGE_LOOP('',(#13000,#13001,#13002,#13003));
#2913=EDGE_LOOP('',(#13004,#13005,#13006,#13007));
#2914=EDGE_LOOP('',(#13008,#13009,#13010,#13011));
#2915=EDGE_LOOP('',(#13012,#13013,#13014,#13015));
#2916=EDGE_LOOP('',(#13016,#13017,#13018,#13019));
#2917=EDGE_LOOP('',(#13020,#13021));
#2918=EDGE_LOOP('',(#13022,#13023,#13024,#13025));
#2919=EDGE_LOOP('',(#13026,#13027,#13028,#13029));
#2920=EDGE_LOOP('',(#13030,#13031,#13032,#13033,#13034,#13035));
#2921=EDGE_LOOP('',(#13036));
#2922=EDGE_LOOP('',(#13037,#13038));
#2923=EDGE_LOOP('',(#13039,#13040,#13041,#13042));
#2924=EDGE_LOOP('',(#13043,#13044,#13045,#13046));
#2925=EDGE_LOOP('',(#13047,#13048,#13049,#13050));
#2926=EDGE_LOOP('',(#13051,#13052,#13053,#13054));
#2927=EDGE_LOOP('',(#13055,#13056,#13057,#13058,#13059));
#2928=EDGE_LOOP('',(#13060));
#2929=EDGE_LOOP('',(#13061,#13062,#13063));
#3434=LINE('',#202427,#3962);
#3435=LINE('',#202431,#3963);
#3436=LINE('',#202435,#3964);
#3437=LINE('',#202440,#3965);
#3438=LINE('',#202443,#3966);
#3439=LINE('',#202449,#3967);
#3440=LINE('',#202453,#3968);
#3441=LINE('',#202456,#3969);
#3442=LINE('',#202460,#3970);
#3443=LINE('',#202464,#3971);
#3444=LINE('',#202473,#3972);
#3445=LINE('',#202476,#3973);
#3446=LINE('',#202481,#3974);
#3447=LINE('',#202485,#3975);
#3448=LINE('',#202490,#3976);
#3449=LINE('',#202492,#3977);
#3450=LINE('',#202493,#3978);
#3451=LINE('',#202495,#3979);
#3452=LINE('',#202504,#3980);
#3453=LINE('',#202506,#3981);
#3454=LINE('',#202507,#3982);
#3455=LINE('',#202512,#3983);
#3456=LINE('',#202519,#3984);
#3457=LINE('',#202524,#3985);
#3458=LINE('',#202525,#3986);
#3459=LINE('',#202526,#3987);
#3962=VECTOR('',#16718,7.55784864301595);
#3963=VECTOR('',#16721,10.);
#3964=VECTOR('',#16724,10.);
#3965=VECTOR('',#16729,10.);
#3966=VECTOR('',#16732,10.);
#3967=VECTOR('',#16737,10.);
#3968=VECTOR('',#16740,10.);
#3969=VECTOR('',#16743,15.2420394990918);
#3970=VECTOR('',#16746,10.);
#3971=VECTOR('',#16749,10.);
#3972=VECTOR('',#16762,10.);
#3973=VECTOR('',#16765,10.);
#3974=VECTOR('',#16770,10.);
#3975=VECTOR('',#16773,10.);
#3976=VECTOR('',#16780,6.50110764916953);
#3977=VECTOR('',#16783,10.);
#3978=VECTOR('',#16784,10.);
#3979=VECTOR('',#16787,10.);
#3980=VECTOR('',#16802,10.);
#3981=VECTOR('',#16803,10.);
#3982=VECTOR('',#16804,10.);
#3983=VECTOR('',#16809,10.);
#3984=VECTOR('',#16818,6.50110764916953);
#3985=VECTOR('',#16823,10.);
#3986=VECTOR('',#16824,10.);
#3987=VECTOR('',#16825,10.);
#4188=CIRCLE('',#15399,7.55784864301595);
#4189=CIRCLE('',#15400,7.55784864301595);
#4190=CIRCLE('',#15401,7.55784864301595);
#4191=CIRCLE('',#15402,7.55784864301595);
#4192=CIRCLE('',#15403,7.55784864301595);
#4193=CIRCLE('',#15404,7.55784864301595);
#4194=CIRCLE('',#15406,15.2420394990918);
#4195=CIRCLE('',#15407,15.2420394990918);
#4196=CIRCLE('',#15408,15.2420394990918);
#4197=CIRCLE('',#15409,15.2420394990918);
#4198=CIRCLE('',#15410,15.2420394990918);
#4199=CIRCLE('',#15411,15.2420394990918);
#4200=CIRCLE('',#15413,7.55784864301595);
#4201=CIRCLE('',#15414,7.55784864301595);
#4202=CIRCLE('',#15416,15.2420394990918);
#4203=CIRCLE('',#15417,15.2420394990918);
#4204=CIRCLE('',#15418,6.50110764916953);
#4205=CIRCLE('',#15420,15.2420394990918);
#4206=CIRCLE('',#15421,15.2420394990918);
#4207=CIRCLE('',#15422,6.50110764916953);
#4208=CIRCLE('',#15430,7.55784864301595);
#4209=CIRCLE('',#15431,7.55784864301595);
#4210=CIRCLE('',#15434,15.2420394990918);
#4211=CIRCLE('',#15435,15.2420394990918);
#4212=CIRCLE('',#15436,6.50110764916953);
#4213=CIRCLE('',#15439,6.50110764916953);
#4214=CIRCLE('',#15442,15.2420394990918);
#4215=CIRCLE('',#15444,15.2420394990918);
#5986=VERTEX_POINT('',#202423);
#5987=VERTEX_POINT('',#202424);
#5988=VERTEX_POINT('',#202426);
#5989=VERTEX_POINT('',#202428);
#5990=VERTEX_POINT('',#202430);
#5991=VERTEX_POINT('',#202432);
#5992=VERTEX_POINT('',#202434);
#5993=VERTEX_POINT('',#202437);
#5994=VERTEX_POINT('',#202439);
#5995=VERTEX_POINT('',#202441);
#5996=VERTEX_POINT('',#202445);
#5997=VERTEX_POINT('',#202446);
#5998=VERTEX_POINT('',#202448);
#5999=VERTEX_POINT('',#202450);
#6000=VERTEX_POINT('',#202452);
#6001=VERTEX_POINT('',#202455);
#6002=VERTEX_POINT('',#202457);
#6003=VERTEX_POINT('',#202459);
#6004=VERTEX_POINT('',#202461);
#6005=VERTEX_POINT('',#202463);
#6006=VERTEX_POINT('',#202470);
#6007=VERTEX_POINT('',#202472);
#6008=VERTEX_POINT('',#202474);
#6009=VERTEX_POINT('',#202477);
#6010=VERTEX_POINT('',#202480);
#6011=VERTEX_POINT('',#202482);
#6012=VERTEX_POINT('',#202484);
#6013=VERTEX_POINT('',#202487);
#6014=VERTEX_POINT('',#202503);
#6015=VERTEX_POINT('',#202505);
#6016=VERTEX_POINT('',#202509);
#6017=VERTEX_POINT('',#202511);
#6018=VERTEX_POINT('',#202514);
#6019=VERTEX_POINT('',#202518);
#6020=VERTEX_POINT('',#202522);
#6021=VERTEX_POINT('',#202523);
#8403=EDGE_CURVE('',#5986,#5987,#4188,.T.);
#8404=EDGE_CURVE('',#5987,#5988,#3434,.T.);
#8405=EDGE_CURVE('',#5989,#5988,#4189,.T.);
#8406=EDGE_CURVE('',#5990,#5989,#3435,.T.);
#8407=EDGE_CURVE('',#5991,#5990,#4190,.T.);
#8408=EDGE_CURVE('',#5992,#5991,#3436,.T.);
#8409=EDGE_CURVE('',#5988,#5992,#4191,.T.);
#8410=EDGE_CURVE('',#5987,#5993,#4192,.T.);
#8411=EDGE_CURVE('',#5994,#5993,#3437,.T.);
#8412=EDGE_CURVE('',#5995,#5994,#4193,.T.);
#8413=EDGE_CURVE('',#5986,#5995,#3438,.T.);
#8414=EDGE_CURVE('',#5996,#5997,#4194,.T.);
#8415=EDGE_CURVE('',#5998,#5996,#3439,.T.);
#8416=EDGE_CURVE('',#5999,#5998,#4195,.T.);
#8417=EDGE_CURVE('',#6000,#5999,#3440,.T.);
#8418=EDGE_CURVE('',#5997,#6000,#4196,.T.);
#8419=EDGE_CURVE('',#5997,#6001,#3441,.T.);
#8420=EDGE_CURVE('',#6002,#6001,#4197,.T.);
#8421=EDGE_CURVE('',#6003,#6002,#3442,.T.);
#8422=EDGE_CURVE('',#6003,#6004,#4198,.T.);
#8423=EDGE_CURVE('',#6005,#6004,#3443,.T.);
#8424=EDGE_CURVE('',#6001,#6005,#4199,.T.);
#8425=EDGE_CURVE('',#5993,#5986,#4200,.T.);
#8426=EDGE_CURVE('',#5994,#5995,#4201,.T.);
#8427=EDGE_CURVE('',#6006,#6003,#4202,.T.);
#8428=EDGE_CURVE('',#6007,#6006,#3444,.T.);
#8429=EDGE_CURVE('',#6008,#6007,#4203,.T.);
#8430=EDGE_CURVE('',#6004,#6008,#3445,.T.);
#8431=EDGE_CURVE('',#6009,#6009,#4204,.T.);
#8432=EDGE_CURVE('',#6005,#6010,#3446,.T.);
#8433=EDGE_CURVE('',#6010,#6011,#4205,.T.);
#8434=EDGE_CURVE('',#6011,#6012,#3447,.T.);
#8435=EDGE_CURVE('',#6012,#6002,#4206,.T.);
#8436=EDGE_CURVE('',#6013,#6013,#4207,.T.);
#8437=EDGE_CURVE('',#6009,#6013,#3448,.T.);
#8438=EDGE_CURVE('',#6006,#6012,#3449,.T.);
#8439=EDGE_CURVE('',#6007,#6011,#3450,.T.);
#8440=EDGE_CURVE('',#6008,#6010,#3451,.T.);
#8441=EDGE_CURVE('',#5991,#5990,#4208,.T.);
#8442=EDGE_CURVE('',#5992,#5989,#4209,.T.);
#8443=EDGE_CURVE('',#5996,#6014,#3452,.T.);
#8444=EDGE_CURVE('',#6015,#6014,#3453,.T.);
#8445=EDGE_CURVE('',#5998,#6015,#3454,.T.);
#8446=EDGE_CURVE('',#6016,#6000,#4210,.T.);
#8447=EDGE_CURVE('',#6017,#6016,#3455,.T.);
#8448=EDGE_CURVE('',#6014,#6017,#4211,.T.);
#8449=EDGE_CURVE('',#6018,#6018,#4212,.T.);
#8450=EDGE_CURVE('',#6018,#6019,#3456,.T.);
#8451=EDGE_CURVE('',#6019,#6019,#4213,.T.);
#8452=EDGE_CURVE('',#6020,#6021,#3457,.T.);
#8453=EDGE_CURVE('',#6020,#6017,#3458,.T.);
#8454=EDGE_CURVE('',#6021,#6016,#3459,.T.);
#8455=EDGE_CURVE('',#6015,#6020,#4214,.T.);
#8456=EDGE_CURVE('',#6021,#5999,#4215,.T.);
#12956=ORIENTED_EDGE('',*,*,#8403,.T.);
#12957=ORIENTED_EDGE('',*,*,#8404,.T.);
#12958=ORIENTED_EDGE('',*,*,#8405,.F.);
#12959=ORIENTED_EDGE('',*,*,#8406,.F.);
#12960=ORIENTED_EDGE('',*,*,#8407,.F.);
#12961=ORIENTED_EDGE('',*,*,#8408,.F.);
#12962=ORIENTED_EDGE('',*,*,#8409,.F.);
#12963=ORIENTED_EDGE('',*,*,#8404,.F.);
#12964=ORIENTED_EDGE('',*,*,#8410,.T.);
#12965=ORIENTED_EDGE('',*,*,#8411,.F.);
#12966=ORIENTED_EDGE('',*,*,#8412,.F.);
#12967=ORIENTED_EDGE('',*,*,#8413,.F.);
#12968=ORIENTED_EDGE('',*,*,#8414,.F.);
#12969=ORIENTED_EDGE('',*,*,#8415,.F.);
#12970=ORIENTED_EDGE('',*,*,#8416,.F.);
#12971=ORIENTED_EDGE('',*,*,#8417,.F.);
#12972=ORIENTED_EDGE('',*,*,#8418,.F.);
#12973=ORIENTED_EDGE('',*,*,#8419,.T.);
#12974=ORIENTED_EDGE('',*,*,#8420,.F.);
#12975=ORIENTED_EDGE('',*,*,#8421,.F.);
#12976=ORIENTED_EDGE('',*,*,#8422,.T.);
#12977=ORIENTED_EDGE('',*,*,#8423,.F.);
#12978=ORIENTED_EDGE('',*,*,#8424,.F.);
#12979=ORIENTED_EDGE('',*,*,#8419,.F.);
#12980=ORIENTED_EDGE('',*,*,#8411,.T.);
#12981=ORIENTED_EDGE('',*,*,#8425,.T.);
#12982=ORIENTED_EDGE('',*,*,#8413,.T.);
#12983=ORIENTED_EDGE('',*,*,#8426,.F.);
#12984=ORIENTED_EDGE('',*,*,#8422,.F.);
#12985=ORIENTED_EDGE('',*,*,#8427,.F.);
#12986=ORIENTED_EDGE('',*,*,#8428,.F.);
#12987=ORIENTED_EDGE('',*,*,#8429,.F.);
#12988=ORIENTED_EDGE('',*,*,#8430,.F.);
#12989=ORIENTED_EDGE('',*,*,#8431,.F.);
#12990=ORIENTED_EDGE('',*,*,#8425,.F.);
#12991=ORIENTED_EDGE('',*,*,#8410,.F.);
#12992=ORIENTED_EDGE('',*,*,#8403,.F.);
#12993=ORIENTED_EDGE('',*,*,#8420,.T.);
#12994=ORIENTED_EDGE('',*,*,#8424,.T.);
#12995=ORIENTED_EDGE('',*,*,#8432,.T.);
#12996=ORIENTED_EDGE('',*,*,#8433,.T.);
#12997=ORIENTED_EDGE('',*,*,#8434,.T.);
#12998=ORIENTED_EDGE('',*,*,#8435,.T.);
#12999=ORIENTED_EDGE('',*,*,#8436,.T.);
#13000=ORIENTED_EDGE('',*,*,#8431,.T.);
#13001=ORIENTED_EDGE('',*,*,#8437,.T.);
#13002=ORIENTED_EDGE('',*,*,#8436,.F.);
#13003=ORIENTED_EDGE('',*,*,#8437,.F.);
#13004=ORIENTED_EDGE('',*,*,#8428,.T.);
#13005=ORIENTED_EDGE('',*,*,#8438,.T.);
#13006=ORIENTED_EDGE('',*,*,#8434,.F.);
#13007=ORIENTED_EDGE('',*,*,#8439,.F.);
#13008=ORIENTED_EDGE('',*,*,#8429,.T.);
#13009=ORIENTED_EDGE('',*,*,#8439,.T.);
#13010=ORIENTED_EDGE('',*,*,#8433,.F.);
#13011=ORIENTED_EDGE('',*,*,#8440,.F.);
#13012=ORIENTED_EDGE('',*,*,#8423,.T.);
#13013=ORIENTED_EDGE('',*,*,#8430,.T.);
#13014=ORIENTED_EDGE('',*,*,#8440,.T.);
#13015=ORIENTED_EDGE('',*,*,#8432,.F.);
#13016=ORIENTED_EDGE('',*,*,#8421,.T.);
#13017=ORIENTED_EDGE('',*,*,#8435,.F.);
#13018=ORIENTED_EDGE('',*,*,#8438,.F.);
#13019=ORIENTED_EDGE('',*,*,#8427,.T.);
#13020=ORIENTED_EDGE('',*,*,#8412,.T.);
#13021=ORIENTED_EDGE('',*,*,#8426,.T.);
#13022=ORIENTED_EDGE('',*,*,#8408,.T.);
#13023=ORIENTED_EDGE('',*,*,#8441,.T.);
#13024=ORIENTED_EDGE('',*,*,#8406,.T.);
#13025=ORIENTED_EDGE('',*,*,#8442,.F.);
#13026=ORIENTED_EDGE('',*,*,#8415,.T.);
#13027=ORIENTED_EDGE('',*,*,#8443,.T.);
#13028=ORIENTED_EDGE('',*,*,#8444,.F.);
#13029=ORIENTED_EDGE('',*,*,#8445,.F.);
#13030=ORIENTED_EDGE('',*,*,#8414,.T.);
#13031=ORIENTED_EDGE('',*,*,#8418,.T.);
#13032=ORIENTED_EDGE('',*,*,#8446,.F.);
#13033=ORIENTED_EDGE('',*,*,#8447,.F.);
#13034=ORIENTED_EDGE('',*,*,#8448,.F.);
#13035=ORIENTED_EDGE('',*,*,#8443,.F.);
#13036=ORIENTED_EDGE('',*,*,#8449,.F.);
#13037=ORIENTED_EDGE('',*,*,#8407,.T.);
#13038=ORIENTED_EDGE('',*,*,#8441,.F.);
#13039=ORIENTED_EDGE('',*,*,#8449,.T.);
#13040=ORIENTED_EDGE('',*,*,#8450,.T.);
#13041=ORIENTED_EDGE('',*,*,#8451,.F.);
#13042=ORIENTED_EDGE('',*,*,#8450,.F.);
#13043=ORIENTED_EDGE('',*,*,#8452,.F.);
#13044=ORIENTED_EDGE('',*,*,#8453,.T.);
#13045=ORIENTED_EDGE('',*,*,#8447,.T.);
#13046=ORIENTED_EDGE('',*,*,#8454,.F.);
#13047=ORIENTED_EDGE('',*,*,#8455,.F.);
#13048=ORIENTED_EDGE('',*,*,#8444,.T.);
#13049=ORIENTED_EDGE('',*,*,#8448,.T.);
#13050=ORIENTED_EDGE('',*,*,#8453,.F.);
#13051=ORIENTED_EDGE('',*,*,#8417,.T.);
#13052=ORIENTED_EDGE('',*,*,#8456,.F.);
#13053=ORIENTED_EDGE('',*,*,#8454,.T.);
#13054=ORIENTED_EDGE('',*,*,#8446,.T.);
#13055=ORIENTED_EDGE('',*,*,#8445,.T.);
#13056=ORIENTED_EDGE('',*,*,#8455,.T.);
#13057=ORIENTED_EDGE('',*,*,#8452,.T.);
#13058=ORIENTED_EDGE('',*,*,#8456,.T.);
#13059=ORIENTED_EDGE('',*,*,#8416,.T.);
#13060=ORIENTED_EDGE('',*,*,#8451,.T.);
#13061=ORIENTED_EDGE('',*,*,#8442,.T.);
#13062=ORIENTED_EDGE('',*,*,#8405,.T.);
#13063=ORIENTED_EDGE('',*,*,#8409,.T.);
#14378=CYLINDRICAL_SURFACE('',#15398,7.55784864301595);
#14379=CYLINDRICAL_SURFACE('',#15405,15.2420394990918);
#14380=CYLINDRICAL_SURFACE('',#15412,7.55784864301595);
#14381=CYLINDRICAL_SURFACE('',#15423,6.50110764916953);
#14382=CYLINDRICAL_SURFACE('',#15425,15.2420394990918);
#14383=CYLINDRICAL_SURFACE('',#15427,15.2420394990918);
#14384=CYLINDRICAL_SURFACE('',#15429,7.55784864301595);
#14385=CYLINDRICAL_SURFACE('',#15438,6.50110764916953);
#14386=CYLINDRICAL_SURFACE('',#15441,15.2420394990918);
#14387=CYLINDRICAL_SURFACE('',#15443,15.2420394990918);
#14781=ADVANCED_FACE('',(#2423),#14378,.F.);
#14782=ADVANCED_FACE('',(#2424),#14379,.T.);
#14783=ADVANCED_FACE('',(#2425),#14380,.F.);
#14784=ADVANCED_FACE('',(#2426,#1989,#1990),#2051,.F.);
#14785=ADVANCED_FACE('',(#2427,#1991),#2052,.T.);
#14786=ADVANCED_FACE('',(#2428),#14381,.F.);
#14787=ADVANCED_FACE('',(#2429),#2053,.T.);
#14788=ADVANCED_FACE('',(#2430),#14382,.T.);
#14789=ADVANCED_FACE('',(#2431),#2054,.T.);
#14790=ADVANCED_FACE('',(#2432),#14383,.T.);
#14791=ADVANCED_FACE('',(#2433),#2055,.T.);
#14792=ADVANCED_FACE('',(#2434),#14384,.F.);
#14793=ADVANCED_FACE('',(#2435),#2056,.F.);
#14794=ADVANCED_FACE('',(#2436,#1992),#2057,.F.);
#14795=ADVANCED_FACE('',(#2437),#2058,.F.);
#14796=ADVANCED_FACE('',(#2438),#14385,.F.);
#14797=ADVANCED_FACE('',(#2439),#2059,.F.);
#14798=ADVANCED_FACE('',(#2440),#14386,.T.);
#14799=ADVANCED_FACE('',(#2441),#14387,.T.);
#14800=ADVANCED_FACE('',(#2442,#1993,#1994),#2060,.T.);
#14940=CLOSED_SHELL('',(#14781,#14782,#14783,#14784,#14785,#14786,#14787,
#14788,#14789,#14790,#14791,#14792,#14793,#14794,#14795,#14796,#14797,#14798,
#14799,#14800));
#15397=AXIS2_PLACEMENT_3D('',#202421,#16712,#16713);
#15398=AXIS2_PLACEMENT_3D('',#202422,#16714,#16715);
#15399=AXIS2_PLACEMENT_3D('',#202425,#16716,#16717);
#15400=AXIS2_PLACEMENT_3D('',#202429,#16719,#16720);
#15401=AXIS2_PLACEMENT_3D('',#202433,#16722,#16723);
#15402=AXIS2_PLACEMENT_3D('',#202436,#16725,#16726);
#15403=AXIS2_PLACEMENT_3D('',#202438,#16727,#16728);
#15404=AXIS2_PLACEMENT_3D('',#202442,#16730,#16731);
#15405=AXIS2_PLACEMENT_3D('',#202444,#16733,#16734);
#15406=AXIS2_PLACEMENT_3D('',#202447,#16735,#16736);
#15407=AXIS2_PLACEMENT_3D('',#202451,#16738,#16739);
#15408=AXIS2_PLACEMENT_3D('',#202454,#16741,#16742);
#15409=AXIS2_PLACEMENT_3D('',#202458,#16744,#16745);
#15410=AXIS2_PLACEMENT_3D('',#202462,#16747,#16748);
#15411=AXIS2_PLACEMENT_3D('',#202465,#16750,#16751);
#15412=AXIS2_PLACEMENT_3D('',#202466,#16752,#16753);
#15413=AXIS2_PLACEMENT_3D('',#202467,#16754,#16755);
#15414=AXIS2_PLACEMENT_3D('',#202468,#16756,#16757);
#15415=AXIS2_PLACEMENT_3D('',#202469,#16758,#16759);
#15416=AXIS2_PLACEMENT_3D('',#202471,#16760,#16761);
#15417=AXIS2_PLACEMENT_3D('',#202475,#16763,#16764);
#15418=AXIS2_PLACEMENT_3D('',#202478,#16766,#16767);
#15419=AXIS2_PLACEMENT_3D('',#202479,#16768,#16769);
#15420=AXIS2_PLACEMENT_3D('',#202483,#16771,#16772);
#15421=AXIS2_PLACEMENT_3D('',#202486,#16774,#16775);
#15422=AXIS2_PLACEMENT_3D('',#202488,#16776,#16777);
#15423=AXIS2_PLACEMENT_3D('',#202489,#16778,#16779);
#15424=AXIS2_PLACEMENT_3D('',#202491,#16781,#16782);
#15425=AXIS2_PLACEMENT_3D('',#202494,#16785,#16786);
#15426=AXIS2_PLACEMENT_3D('',#202496,#16788,#16789);
#15427=AXIS2_PLACEMENT_3D('',#202497,#16790,#16791);
#15428=AXIS2_PLACEMENT_3D('',#202498,#16792,#16793);
#15429=AXIS2_PLACEMENT_3D('',#202499,#16794,#16795);
#15430=AXIS2_PLACEMENT_3D('',#202500,#16796,#16797);
#15431=AXIS2_PLACEMENT_3D('',#202501,#16798,#16799);
#15432=AXIS2_PLACEMENT_3D('',#202502,#16800,#16801);
#15433=AXIS2_PLACEMENT_3D('',#202508,#16805,#16806);
#15434=AXIS2_PLACEMENT_3D('',#202510,#16807,#16808);
#15435=AXIS2_PLACEMENT_3D('',#202513,#16810,#16811);
#15436=AXIS2_PLACEMENT_3D('',#202515,#16812,#16813);
#15437=AXIS2_PLACEMENT_3D('',#202516,#16814,#16815);
#15438=AXIS2_PLACEMENT_3D('',#202517,#16816,#16817);
#15439=AXIS2_PLACEMENT_3D('',#202520,#16819,#16820);
#15440=AXIS2_PLACEMENT_3D('',#202521,#16821,#16822);
#15441=AXIS2_PLACEMENT_3D('',#202527,#16826,#16827);
#15442=AXIS2_PLACEMENT_3D('',#202528,#16828,#16829);
#15443=AXIS2_PLACEMENT_3D('',#202529,#16830,#16831);
#15444=AXIS2_PLACEMENT_3D('',#202530,#16832,#16833);
#15445=AXIS2_PLACEMENT_3D('',#202531,#16834,#16835);
#16712=DIRECTION('axis',(0.,0.,1.));
#16713=DIRECTION('refdir',(1.,0.,0.));
#16714=DIRECTION('center_axis',(0.,-1.,0.));
#16715=DIRECTION('ref_axis',(-1.,0.,0.));
#16716=DIRECTION('center_axis',(0.,1.,0.));
#16717=DIRECTION('ref_axis',(-1.,0.,0.));
#16718=DIRECTION('',(0.,-1.,0.));
#16719=DIRECTION('center_axis',(0.,1.,0.));
#16720=DIRECTION('ref_axis',(-1.,0.,0.));
#16721=DIRECTION('',(0.,-1.,0.));
#16722=DIRECTION('center_axis',(0.,1.,0.));
#16723=DIRECTION('ref_axis',(-1.,0.,0.));
#16724=DIRECTION('',(0.,1.,0.));
#16725=DIRECTION('center_axis',(0.,1.,0.));
#16726=DIRECTION('ref_axis',(-1.,0.,0.));
#16727=DIRECTION('center_axis',(0.,1.,0.));
#16728=DIRECTION('ref_axis',(-1.,0.,0.));
#16729=DIRECTION('',(0.,1.,0.));
#16730=DIRECTION('center_axis',(0.,-1.,0.));
#16731=DIRECTION('ref_axis',(-1.,0.,0.));
#16732=DIRECTION('',(0.,-1.,0.));
#16733=DIRECTION('center_axis',(0.,-1.,0.));
#16734=DIRECTION('ref_axis',(-1.,0.,0.));
#16735=DIRECTION('center_axis',(0.,-1.,0.));
#16736=DIRECTION('ref_axis',(-1.,0.,0.));
#16737=DIRECTION('',(0.,1.,0.));
#16738=DIRECTION('center_axis',(0.,-1.,0.));
#16739=DIRECTION('ref_axis',(-1.,0.,0.));
#16740=DIRECTION('',(0.,-1.,0.));
#16741=DIRECTION('center_axis',(0.,-1.,0.));
#16742=DIRECTION('ref_axis',(-1.,0.,0.));
#16743=DIRECTION('',(0.,1.,0.));
#16744=DIRECTION('center_axis',(0.,1.,0.));
#16745=DIRECTION('ref_axis',(-1.,0.,0.));
#16746=DIRECTION('',(0.,-1.,0.));
#16747=DIRECTION('center_axis',(0.,-1.,0.));
#16748=DIRECTION('ref_axis',(-1.,0.,0.));
#16749=DIRECTION('',(0.,1.,0.));
#16750=DIRECTION('center_axis',(0.,1.,0.));
#16751=DIRECTION('ref_axis',(-1.,0.,0.));
#16752=DIRECTION('center_axis',(0.,-1.,0.));
#16753=DIRECTION('ref_axis',(-0.503773977045354,0.,0.863835505204496));
#16754=DIRECTION('center_axis',(-1.19937668507924E-53,1.,-2.1198911140988E-53));
#16755=DIRECTION('ref_axis',(-0.492423560103467,-2.43566064310008E-53,-0.8703556959399));
#16756=DIRECTION('center_axis',(-1.19937668507924E-53,1.,-2.1198911140988E-53));
#16757=DIRECTION('ref_axis',(-0.492423560103467,-2.43566064310008E-53,-0.8703556959399));
#16758=DIRECTION('center_axis',(0.,-1.,0.));
#16759=DIRECTION('ref_axis',(-0.492423560103467,0.,-0.8703556959399));
#16760=DIRECTION('center_axis',(0.,-1.,0.));
#16761=DIRECTION('ref_axis',(0.503443599526488,0.,-0.864028091033974));
#16762=DIRECTION('',(0.864028091033974,0.,0.503443599526487));
#16763=DIRECTION('center_axis',(0.,-1.,0.));
#16764=DIRECTION('ref_axis',(-0.503443599526489,0.,0.864028091033974));
#16765=DIRECTION('',(-0.864028091033974,0.,-0.503443599526487));
#16766=DIRECTION('center_axis',(0.,1.,0.));
#16767=DIRECTION('ref_axis',(-0.492423560103467,0.,-0.8703556959399));
#16768=DIRECTION('center_axis',(0.,-1.,0.));
#16769=DIRECTION('ref_axis',(-0.492423560103467,0.,-0.8703556959399));
#16770=DIRECTION('',(-0.864028091033974,0.,-0.503443599526487));
#16771=DIRECTION('center_axis',(0.,-1.,0.));
#16772=DIRECTION('ref_axis',(-0.503443599526489,0.,0.864028091033974));
#16773=DIRECTION('',(0.864028091033974,0.,0.503443599526487));
#16774=DIRECTION('center_axis',(0.,-1.,0.));
#16775=DIRECTION('ref_axis',(0.503443599526488,0.,-0.864028091033974));
#16776=DIRECTION('center_axis',(0.,1.,0.));
#16777=DIRECTION('ref_axis',(-0.492423560103467,0.,-0.8703556959399));
#16778=DIRECTION('center_axis',(0.,-1.,0.));
#16779=DIRECTION('ref_axis',(-0.492423560103467,0.,-0.8703556959399));
#16780=DIRECTION('',(0.,-1.,0.));
#16781=DIRECTION('center_axis',(0.503443599526487,0.,-0.864028091033974));
#16782=DIRECTION('ref_axis',(0.864028091033974,0.,0.503443599526487));
#16783=DIRECTION('',(0.,-1.,0.));
#16784=DIRECTION('',(0.,-1.,0.));
#16785=DIRECTION('center_axis',(0.,-1.,0.));
#16786=DIRECTION('ref_axis',(-0.503443599526489,0.,0.864028091033974));
#16787=DIRECTION('',(0.,-1.,0.));
#16788=DIRECTION('center_axis',(-0.503443599526487,0.,0.864028091033974));
#16789=DIRECTION('ref_axis',(-0.864028091033974,0.,-0.503443599526487));
#16790=DIRECTION('center_axis',(0.,-1.,0.));
#16791=DIRECTION('ref_axis',(0.503443599526488,0.,-0.864028091033974));
#16792=DIRECTION('center_axis',(0.,-1.,0.));
#16793=DIRECTION('ref_axis',(-0.492423560103467,0.,-0.8703556959399));
#16794=DIRECTION('center_axis',(0.,-1.,0.));
#16795=DIRECTION('ref_axis',(-0.503773977045354,0.,0.863835505204496));
#16796=DIRECTION('center_axis',(1.19937668507924E-53,1.,2.1198911140988E-53));
#16797=DIRECTION('ref_axis',(-0.492423560103467,2.43566064310008E-53,-0.8703556959399));
#16798=DIRECTION('center_axis',(1.19937668507924E-53,1.,2.1198911140988E-53));
#16799=DIRECTION('ref_axis',(-0.492423560103467,2.43566064310008E-53,-0.8703556959399));
#16800=DIRECTION('center_axis',(0.503443599526487,0.,-0.864028091033974));
#16801=DIRECTION('ref_axis',(-0.864028091033974,0.,-0.503443599526487));
#16802=DIRECTION('',(-0.864028091033974,0.,-0.503443599526487));
#16803=DIRECTION('',(0.,1.,0.));
#16804=DIRECTION('',(-0.864028091033974,0.,-0.503443599526487));
#16805=DIRECTION('center_axis',(0.,-1.,0.));
#16806=DIRECTION('ref_axis',(-0.492423560103467,0.,-0.8703556959399));
#16807=DIRECTION('center_axis',(0.,-1.,0.));
#16808=DIRECTION('ref_axis',(0.503443599526488,0.,-0.864028091033974));
#16809=DIRECTION('',(0.864028091033974,0.,0.503443599526487));
#16810=DIRECTION('center_axis',(0.,-1.,0.));
#16811=DIRECTION('ref_axis',(-0.503443599526489,0.,0.864028091033974));
#16812=DIRECTION('center_axis',(0.,1.,0.));
#16813=DIRECTION('ref_axis',(-0.492423560103467,0.,-0.8703556959399));
#16814=DIRECTION('center_axis',(0.,-1.,0.));
#16815=DIRECTION('ref_axis',(-0.492423560103467,0.,-0.8703556959399));
#16816=DIRECTION('center_axis',(0.,-1.,0.));
#16817=DIRECTION('ref_axis',(-0.492423560103467,0.,-0.8703556959399));
#16818=DIRECTION('',(0.,-1.,0.));
#16819=DIRECTION('center_axis',(0.,1.,0.));
#16820=DIRECTION('ref_axis',(-0.492423560103467,0.,-0.8703556959399));
#16821=DIRECTION('center_axis',(-0.503443599526487,0.,0.864028091033974));
#16822=DIRECTION('ref_axis',(0.864028091033974,0.,0.503443599526487));
#16823=DIRECTION('',(0.864028091033974,0.,0.503443599526487));
#16824=DIRECTION('',(0.,1.,0.));
#16825=DIRECTION('',(0.,1.,0.));
#16826=DIRECTION('center_axis',(0.,-1.,0.));
#16827=DIRECTION('ref_axis',(-0.503443599526489,0.,0.864028091033974));
#16828=DIRECTION('center_axis',(0.,-1.,0.));
#16829=DIRECTION('ref_axis',(-0.503443599526489,0.,0.864028091033974));
#16830=DIRECTION('center_axis',(0.,-1.,0.));
#16831=DIRECTION('ref_axis',(0.503443599526488,0.,-0.864028091033974));
#16832=DIRECTION('center_axis',(0.,-1.,0.));
#16833=DIRECTION('ref_axis',(0.503443599526488,0.,-0.864028091033974));
#16834=DIRECTION('center_axis',(0.,-1.,0.));
#16835=DIRECTION('ref_axis',(-0.492423560103467,0.,-0.8703556959399));
#202421=CARTESIAN_POINT('',(0.,0.,0.));
#202422=CARTESIAN_POINT('Origin',(-19.9792411332937,17.,231.631408332131));
#202423=CARTESIAN_POINT('',(-13.4123053085775,17.,235.37258862514));
#202424=CARTESIAN_POINT('',(-12.4213924902778,17.,231.631408332131));
#202425=CARTESIAN_POINT('Origin',(-19.9792411332937,17.,231.631408332131));
#202426=CARTESIAN_POINT('',(-12.4213924902778,-17.,231.631408332131));
#202427=CARTESIAN_POINT('',(-12.4213924902778,17.,231.631408332131));
#202428=CARTESIAN_POINT('',(-13.4123053085775,-17.,235.37258862514));
#202429=CARTESIAN_POINT('Origin',(-19.9792411332937,-17.,231.631408332131));
#202430=CARTESIAN_POINT('',(-13.4123053085775,-12.,235.37258862514));
#202431=CARTESIAN_POINT('',(-13.4123053085775,17.,235.37258862514));
#202432=CARTESIAN_POINT('',(-26.4691126286313,-12.,227.758083651093));
#202433=CARTESIAN_POINT('Origin',(-19.9792411332937,-12.,231.631408332131));
#202434=CARTESIAN_POINT('',(-26.4691126286313,-17.,227.758083651093));
#202435=CARTESIAN_POINT('',(-26.4691126286313,17.,227.758083651093));
#202436=CARTESIAN_POINT('Origin',(-19.9792411332937,-17.,231.631408332131));
#202437=CARTESIAN_POINT('',(-26.4691126286313,17.,227.758083651093));
#202438=CARTESIAN_POINT('Origin',(-19.9792411332937,17.,231.631408332131));
#202439=CARTESIAN_POINT('',(-26.4691126286313,12.,227.758083651093));
#202440=CARTESIAN_POINT('',(-26.4691126286313,17.,227.758083651093));
#202441=CARTESIAN_POINT('',(-13.4123053085775,12.,235.37258862514));
#202442=CARTESIAN_POINT('Origin',(-19.9792411332937,12.,231.631408332131));
#202443=CARTESIAN_POINT('',(-13.4123053085775,17.,235.37258862514));
#202444=CARTESIAN_POINT('Origin',(-19.9792411332937,17.,231.631408332131));
#202445=CARTESIAN_POINT('',(-29.4368821049519,-12.,243.584349198005));
#202446=CARTESIAN_POINT('',(-4.7372016342019,-12.,231.631408332131));
#202447=CARTESIAN_POINT('Origin',(-19.9792411332937,-12.,231.631408332131));
#202448=CARTESIAN_POINT('',(-29.4368821049519,-17.,243.584349198005));
#202449=CARTESIAN_POINT('',(-29.4368821049519,17.,243.584349198005));
#202450=CARTESIAN_POINT('',(-6.77425985905829,-17.,239.243782313943));
#202451=CARTESIAN_POINT('Origin',(-19.9792411332937,-17.,231.631408332131));
#202452=CARTESIAN_POINT('',(-6.77425985905829,-12.,239.243782313943));
#202453=CARTESIAN_POINT('',(-6.77425985905829,17.,239.243782313943));
#202454=CARTESIAN_POINT('Origin',(-19.9792411332937,-12.,231.631408332131));
#202455=CARTESIAN_POINT('',(-4.7372016342019,12.,231.631408332131));
#202456=CARTESIAN_POINT('',(-4.7372016342019,17.,231.631408332131));
#202457=CARTESIAN_POINT('',(-6.77425985905829,12.,239.243782313943));
#202458=CARTESIAN_POINT('Origin',(-19.9792411332937,12.,231.631408332131));
#202459=CARTESIAN_POINT('',(-6.77425985905829,17.,239.243782313943));
#202460=CARTESIAN_POINT('',(-6.77425985905829,17.,239.243782313943));
#202461=CARTESIAN_POINT('',(-29.4368821049519,17.,243.584349198005));
#202462=CARTESIAN_POINT('Origin',(-19.9792411332937,17.,231.631408332131));
#202463=CARTESIAN_POINT('',(-29.4368821049519,12.,243.584349198005));
#202464=CARTESIAN_POINT('',(-29.4368821049519,17.,243.584349198005));
#202465=CARTESIAN_POINT('Origin',(-19.9792411332937,12.,231.631408332131));
#202466=CARTESIAN_POINT('Origin',(-19.9021768039151,17.,231.499263944101));
#202467=CARTESIAN_POINT('Origin',(-19.9021768039151,17.,231.499263944101));
#202468=CARTESIAN_POINT('Origin',(-19.9021768039151,12.,231.499263944101));
#202469=CARTESIAN_POINT('Origin',(-106.310292012757,17.,181.151812280833));
#202470=CARTESIAN_POINT('',(-12.2286695743674,17.,218.329713652237));
#202471=CARTESIAN_POINT('Origin',(-19.9021768039151,17.,231.499263944101));
#202472=CARTESIAN_POINT('',(-185.044899992051,17.,117.634810325701));
#202473=CARTESIAN_POINT('',(-185.044899992051,17.,117.634810325701));
#202474=CARTESIAN_POINT('',(-200.391914451146,17.,143.97391090943));
#202475=CARTESIAN_POINT('Origin',(-192.718407221598,17.,130.804360617566));
#202476=CARTESIAN_POINT('',(-27.5756840334628,17.,244.668814235966));
#202477=CARTESIAN_POINT('',(-189.517108648379,17.,136.462636689939));
#202478=CARTESIAN_POINT('Origin',(-192.718407221598,17.,130.804360617566));
#202479=CARTESIAN_POINT('Origin',(-106.310292012757,12.,181.151812280833));
#202480=CARTESIAN_POINT('',(-200.391914451146,12.,143.97391090943));
#202481=CARTESIAN_POINT('',(-27.5756840334628,12.,244.668814235966));
#202482=CARTESIAN_POINT('',(-185.044899992051,12.,117.634810325701));
#202483=CARTESIAN_POINT('Origin',(-192.718407221598,12.,130.804360617566));
#202484=CARTESIAN_POINT('',(-12.2286695743674,12.,218.329713652237));
#202485=CARTESIAN_POINT('',(-185.044899992051,12.,117.634810325701));
#202486=CARTESIAN_POINT('Origin',(-19.9021768039151,12.,231.499263944101));
#202487=CARTESIAN_POINT('',(-189.517108648379,12.,136.462636689939));
#202488=CARTESIAN_POINT('Origin',(-192.718407221598,12.,130.804360617566));
#202489=CARTESIAN_POINT('Origin',(-192.718407221598,17.,130.804360617566));
#202490=CARTESIAN_POINT('',(-189.517108648378,17.,136.462636689939));
#202491=CARTESIAN_POINT('Origin',(-185.044899992051,17.,117.634810325701));
#202492=CARTESIAN_POINT('',(-12.2286695743674,17.,218.329713652237));
#202493=CARTESIAN_POINT('',(-185.044899992051,17.,117.634810325701));
#202494=CARTESIAN_POINT('Origin',(-192.718407221598,17.,130.804360617566));
#202495=CARTESIAN_POINT('',(-200.391914451146,17.,143.97391090943));
#202496=CARTESIAN_POINT('Origin',(-27.5756840334628,17.,244.668814235966));
#202497=CARTESIAN_POINT('Origin',(-19.9021768039151,17.,231.499263944101));
#202498=CARTESIAN_POINT('Origin',(-106.310292012757,12.,181.151812280833));
#202499=CARTESIAN_POINT('Origin',(-19.9021768039151,-17.,231.499263944101));
#202500=CARTESIAN_POINT('Origin',(-19.9021768039151,-12.,231.499263944101));
#202501=CARTESIAN_POINT('Origin',(-19.9021768039151,-17.,231.499263944101));
#202502=CARTESIAN_POINT('Origin',(-27.5756840334628,-17.,244.668814235966));
#202503=CARTESIAN_POINT('',(-200.391914451146,-12.,143.97391090943));
#202504=CARTESIAN_POINT('',(-27.5756840334628,-12.,244.668814235966));
#202505=CARTESIAN_POINT('',(-200.391914451146,-17.,143.97391090943));
#202506=CARTESIAN_POINT('',(-200.391914451146,-17.,143.97391090943));
#202507=CARTESIAN_POINT('',(-27.5756840334628,-17.,244.668814235966));
#202508=CARTESIAN_POINT('Origin',(-106.310292012757,-12.,181.151812280833));
#202509=CARTESIAN_POINT('',(-12.2286695743674,-12.,218.329713652237));
#202510=CARTESIAN_POINT('Origin',(-19.9021768039151,-12.,231.499263944101));
#202511=CARTESIAN_POINT('',(-185.044899992051,-12.,117.634810325701));
#202512=CARTESIAN_POINT('',(-185.044899992051,-12.,117.634810325701));
#202513=CARTESIAN_POINT('Origin',(-192.718407221598,-12.,130.804360617566));
#202514=CARTESIAN_POINT('',(-189.517108648379,-12.,136.462636689939));
#202515=CARTESIAN_POINT('Origin',(-192.718407221598,-12.,130.804360617566));
#202516=CARTESIAN_POINT('Origin',(-106.310292012757,-12.,181.151812280833));
#202517=CARTESIAN_POINT('Origin',(-192.718407221598,-17.,130.804360617566));
#202518=CARTESIAN_POINT('',(-189.517108648379,-17.,136.462636689939));
#202519=CARTESIAN_POINT('',(-189.517108648378,-17.,136.462636689939));
#202520=CARTESIAN_POINT('Origin',(-192.718407221598,-17.,130.804360617566));
#202521=CARTESIAN_POINT('Origin',(-185.044899992051,-17.,117.634810325701));
#202522=CARTESIAN_POINT('',(-185.044899992051,-17.,117.634810325701));
#202523=CARTESIAN_POINT('',(-12.2286695743674,-17.,218.329713652237));
#202524=CARTESIAN_POINT('',(-185.044899992051,-17.,117.634810325701));
#202525=CARTESIAN_POINT('',(-185.044899992051,-17.,117.634810325701));
#202526=CARTESIAN_POINT('',(-12.2286695743674,-17.,218.329713652237));
#202527=CARTESIAN_POINT('Origin',(-192.718407221598,-17.,130.804360617566));
#202528=CARTESIAN_POINT('Origin',(-192.718407221598,-17.,130.804360617566));
#202529=CARTESIAN_POINT('Origin',(-19.9021768039151,-17.,231.499263944101));
#202530=CARTESIAN_POINT('Origin',(-19.9021768039151,-17.,231.499263944101));
#202531=CARTESIAN_POINT('Origin',(-106.310292012757,-17.,181.151812280833));
#279248=UNCERTAINTY_MEASURE_WITH_UNIT(LENGTH_MEASURE(0.01),#279267,
'DISTANCE_ACCURACY_VALUE',
'Maximum model space distance between geometric entities at asserted c
onnectivities');
#279255=UNCERTAINTY_MEASURE_WITH_UNIT(LENGTH_MEASURE(0.01),#279267,
'DISTANCE_ACCURACY_VALUE',
'Maximum model space distance between geometric entities at asserted c
onnectivities');
#279259=(
GEOMETRIC_REPRESENTATION_CONTEXT(3)
GLOBAL_UNCERTAINTY_ASSIGNED_CONTEXT((#279248))
GLOBAL_UNIT_ASSIGNED_CONTEXT((#279267,#279269,#279270))
REPRESENTATION_CONTEXT('','3D')
);
#279266=(
GEOMETRIC_REPRESENTATION_CONTEXT(3)
GLOBAL_UNCERTAINTY_ASSIGNED_CONTEXT((#279255))
GLOBAL_UNIT_ASSIGNED_CONTEXT((#279267,#279269,#279270))
REPRESENTATION_CONTEXT('','3D')
);
#279267=(
LENGTH_UNIT()
NAMED_UNIT(*)
SI_UNIT(.MILLI.,.METRE.)
);
#279269=(
NAMED_UNIT(*)
PLANE_ANGLE_UNIT()
SI_UNIT($,.RADIAN.)
);
#279270=(
NAMED_UNIT(*)
SI_UNIT($,.STERADIAN.)
SOLID_ANGLE_UNIT()
);
#279274=SHAPE_DEFINITION_REPRESENTATION(#279284,#279303);
#279284=PRODUCT_DEFINITION_SHAPE('',$,#279314);
#279303=SHAPE_REPRESENTATION('',(#15397),#279259);
#279310=PRODUCT_DEFINITION_CONTEXT('part definition',#279342,'design');
#279314=PRODUCT_DEFINITION('Arm_04','Arm_04',#279324,#279310);
#279324=PRODUCT_DEFINITION_FORMATION('',$,#279347);
#279342=APPLICATION_CONTEXT(
'Core Data for Automotive Mechanical Design Process');
#279343=PRODUCT_CONTEXT('part definition',#279342,'mechanical');
#279347=PRODUCT('Arm_04','Arm_04',$,(#279343));
#279355=PRESENTATION_STYLE_ASSIGNMENT((#279357));
#279357=SURFACE_STYLE_USAGE(.BOTH.,#279359);
#279359=SURFACE_SIDE_STYLE('',(#279361));
#279361=SURFACE_STYLE_FILL_AREA(#279363);
#279363=FILL_AREA_STYLE('Opaque(160,160,160)',(#279365));
#279365=FILL_AREA_STYLE_COLOUR('Opaque(160,160,160)',#279367);
#279367=COLOUR_RGB('Opaque(160,160,160)', 0.66274510, 0.83137255, 0.94901961);
ENDSEC;
END-ISO-10303-21;
